ISO-10303-21;
HEADER;
/* Generated by software containing ST-Developer
 * from STEP Tools, Inc. (www.steptools.com) 
 */

FILE_DESCRIPTION(
/* description */ ('PAT-091'),
/* implementation_level */ '2;1');

FILE_NAME(
/* name */ 'Axle distance sleeve 10 mm (1).step',
/* time_stamp */ '2026-10-27T15:34:44-07:00',
/* author */ (''),
/* organization */ (''),
/* preprocessor_version */ 'ST-DEVELOPER v20.2',
/* originating_system */ 'Autodesk Translation Framework v15.17.0.0',
/* authorisation */ '');

FILE_SCHEMA (('AUTOMOTIVE_DESIGN { 1 0 10303 214 3 1 1 }'));
ENDSEC;

DATA;
#10=MECHANICAL_DESIGN_GEOMETRIC_PRESENTATION_REPRESENTATION('',(#1010),#25100);
#790=SHAPE_REPRESENTATION_RELATIONSHIP('SRR','None',#25553,#900);
#900=ADVANCED_BREP_SHAPE_REPRESENTATION('',(#1132),#25023);
#1010=STYLED_ITEM('',(#26191),#1132);
#1132=MANIFOLD_SOLID_BREP('Body1',#13289);
#1426=FACE_BOUND('',#3419,.T.);
#1427=FACE_BOUND('',#3421,.T.);
#1817=PLANE('',#15248);
#1818=PLANE('',#15249);
#2387=FACE_OUTER_BOUND('',#3416,.T.);
#2388=FACE_OUTER_BOUND('',#3417,.T.);
#2389=FACE_OUTER_BOUND('',#3418,.T.);
#2390=FACE_OUTER_BOUND('',#3420,.T.);
#3416=EDGE_LOOP('',(#10308,#10309,#10310,#10311));
#3417=EDGE_LOOP('',(#10312,#10313,#10314,#10315));
#3418=EDGE_LOOP('',(#10316));
#3419=EDGE_LOOP('',(#10317));
#3420=EDGE_LOOP('',(#10318));
#3421=EDGE_LOOP('',(#10319));
#4501=LINE('',#22483,#5241);
#4502=LINE('',#22489,#5242);
#5241=VECTOR('',#18163,0.604999999999997);
#5242=VECTOR('',#18170,0.799999999999997);
#5893=CIRCLE('',#15243,0.604999999999997);
#5894=CIRCLE('',#15244,0.604999999999997);
#5895=CIRCLE('',#15246,0.799999999999997);
#5896=CIRCLE('',#15247,0.799999999999997);
#6826=VERTEX_POINT('',#22480);
#6827=VERTEX_POINT('',#22482);
#6828=VERTEX_POINT('',#22486);
#6829=VERTEX_POINT('',#22488);
#8089=EDGE_CURVE('',#6826,#6826,#5893,.T.);
#8090=EDGE_CURVE('',#6826,#6827,#4501,.T.);
#8091=EDGE_CURVE('',#6827,#6827,#5894,.T.);
#8092=EDGE_CURVE('',#6828,#6828,#5895,.T.);
#8093=EDGE_CURVE('',#6828,#6829,#4502,.T.);
#8094=EDGE_CURVE('',#6829,#6829,#5896,.T.);
#10308=ORIENTED_EDGE('',*,*,#8089,.F.);
#10309=ORIENTED_EDGE('',*,*,#8090,.T.);
#10310=ORIENTED_EDGE('',*,*,#8091,.T.);
#10311=ORIENTED_EDGE('',*,*,#8090,.F.);
#10312=ORIENTED_EDGE('',*,*,#8092,.F.);
#10313=ORIENTED_EDGE('',*,*,#8093,.T.);
#10314=ORIENTED_EDGE('',*,*,#8094,.T.);
#10315=ORIENTED_EDGE('',*,*,#8093,.F.);
#10316=ORIENTED_EDGE('',*,*,#8092,.T.);
#10317=ORIENTED_EDGE('',*,*,#8089,.T.);
#10318=ORIENTED_EDGE('',*,*,#8094,.F.);
#10319=ORIENTED_EDGE('',*,*,#8091,.F.);
#12214=CYLINDRICAL_SURFACE('',#15242,0.604999999999997);
#12215=CYLINDRICAL_SURFACE('',#15245,0.799999999999997);
#12754=ADVANCED_FACE('',(#2387),#12214,.F.);
#12755=ADVANCED_FACE('',(#2388),#12215,.T.);
#12756=ADVANCED_FACE('',(#2389,#1426),#1817,.T.);
#12757=ADVANCED_FACE('',(#2390,#1427),#1818,.F.);
#13289=CLOSED_SHELL('',(#12754,#12755,#12756,#12757));
#15241=AXIS2_PLACEMENT_3D('',#22478,#18157,#18158);
#15242=AXIS2_PLACEMENT_3D('',#22479,#18159,#18160);
#15243=AXIS2_PLACEMENT_3D('',#22481,#18161,#18162);
#15244=AXIS2_PLACEMENT_3D('',#22484,#18164,#18165);
#15245=AXIS2_PLACEMENT_3D('',#22485,#18166,#18167);
#15246=AXIS2_PLACEMENT_3D('',#22487,#18168,#18169);
#15247=AXIS2_PLACEMENT_3D('',#22490,#18171,#18172);
#15248=AXIS2_PLACEMENT_3D('',#22491,#18173,#18174);
#15249=AXIS2_PLACEMENT_3D('',#22492,#18175,#18176);
#18157=DIRECTION('axis',(0.,0.,1.));
#18158=DIRECTION('refdir',(1.,0.,0.));
#18159=DIRECTION('center_axis',(0.,1.,0.));
#18160=DIRECTION('ref_axis',(1.,0.,0.));
#18161=DIRECTION('center_axis',(0.,-1.,0.));
#18162=DIRECTION('ref_axis',(1.,0.,0.));
#18163=DIRECTION('',(0.,-1.,0.));
#18164=DIRECTION('center_axis',(0.,-1.,0.));
#18165=DIRECTION('ref_axis',(1.,0.,0.));
#18166=DIRECTION('center_axis',(0.,1.,0.));
#18167=DIRECTION('ref_axis',(1.,0.,0.));
#18168=DIRECTION('center_axis',(0.,1.,0.));
#18169=DIRECTION('ref_axis',(1.,0.,0.));
#18170=DIRECTION('',(0.,-1.,0.));
#18171=DIRECTION('center_axis',(0.,1.,0.));
#18172=DIRECTION('ref_axis',(1.,0.,0.));
#18173=DIRECTION('center_axis',(0.,1.,0.));
#18174=DIRECTION('ref_axis',(1.,0.,0.));
#18175=DIRECTION('center_axis',(0.,1.,0.));
#18176=DIRECTION('ref_axis',(1.,0.,0.));
#22478=CARTESIAN_POINT('',(0.,0.,0.));
#22479=CARTESIAN_POINT('Origin',(38.7298334620742,-4.5,3.));
#22480=CARTESIAN_POINT('',(38.1248334620742,-3.5,3.));
#22481=CARTESIAN_POINT('Origin',(38.7298334620742,-3.5,3.));
#22482=CARTESIAN_POINT('',(38.1248334620742,-4.5,3.));
#22483=CARTESIAN_POINT('',(38.1248334620742,-4.5,3.));
#22484=CARTESIAN_POINT('Origin',(38.7298334620742,-4.5,3.));
#22485=CARTESIAN_POINT('Origin',(38.7298334620742,-4.5,3.));
#22486=CARTESIAN_POINT('',(37.9298334620742,-3.5,3.));
#22487=CARTESIAN_POINT('Origin',(38.7298334620742,-3.5,3.));
#22488=CARTESIAN_POINT('',(37.9298334620742,-4.5,3.));
#22489=CARTESIAN_POINT('',(37.9298334620742,-4.5,3.));
#22490=CARTESIAN_POINT('Origin',(38.7298334620742,-4.5,3.));
#22491=CARTESIAN_POINT('Origin',(38.7298334620742,-3.5,3.));
#22492=CARTESIAN_POINT('Origin',(38.7298334620742,-4.5,3.));
#24902=UNCERTAINTY_MEASURE_WITH_UNIT(LENGTH_MEASURE(0.001),#25101,
'DISTANCE_ACCURACY_VALUE',
'Maximum model space distance between geometric entities at asserted c
onnectivities');
#24979=UNCERTAINTY_MEASURE_WITH_UNIT(LENGTH_MEASURE(0.001),#25101,
'DISTANCE_ACCURACY_VALUE',
'Maximum model space distance between geometric entities at asserted c
onnectivities');
#25023=(
GEOMETRIC_REPRESENTATION_CONTEXT(3)
GLOBAL_UNCERTAINTY_ASSIGNED_CONTEXT((#24902))
GLOBAL_UNIT_ASSIGNED_CONTEXT((#25101,#25103,#25104))
REPRESENTATION_CONTEXT('','3D')
);
#25100=(
GEOMETRIC_REPRESENTATION_CONTEXT(3)
GLOBAL_UNCERTAINTY_ASSIGNED_CONTEXT((#24979))
GLOBAL_UNIT_ASSIGNED_CONTEXT((#25101,#25103,#25104))
REPRESENTATION_CONTEXT('','3D')
);
#25101=(
LENGTH_UNIT()
NAMED_UNIT(*)
SI_UNIT(.CENTI.,.METRE.)
);
#25103=(
NAMED_UNIT(*)
PLANE_ANGLE_UNIT()
SI_UNIT($,.RADIAN.)
);
#25104=(
NAMED_UNIT(*)
SI_UNIT($,.STERADIAN.)
SOLID_ANGLE_UNIT()
);
#25148=SHAPE_DEFINITION_REPRESENTATION(#25268,#25553);
#25268=PRODUCT_DEFINITION_SHAPE('',$,#25674);
#25553=SHAPE_REPRESENTATION('',(#15241),#25023);
#25630=PRODUCT_DEFINITION_CONTEXT('part definition',#25992,'design');
#25674=PRODUCT_DEFINITION('Axle distance sleeve 10 mm (1)',
'Axle distance sleeve 10 mm (1)',#25794,#25630);
#25794=PRODUCT_DEFINITION_FORMATION('',$,#26037);
#25992=APPLICATION_CONTEXT(
'Core Data for Automotive Mechanical Design Process');
#25993=PRODUCT_CONTEXT('part definition',#25992,'mechanical');
#26037=PRODUCT('Axle distance sleeve 10 mm (1)',
'Axle distance sleeve 10 mm (1)','Axle distance sleeve 10 mm (1)',(#25993));
#26185=COLOUR_RGB('Grey',0.48,0.52,0.57);
#26186=FILL_AREA_STYLE_COLOUR('',#26185);
#26187=FILL_AREA_STYLE('',(#26186));
#26188=SURFACE_STYLE_FILL_AREA(#26187);
#26189=SURFACE_SIDE_STYLE('',(#26188));
#26190=SURFACE_STYLE_USAGE(.BOTH.,#26189);
#26191=PRESENTATION_STYLE_ASSIGNMENT((#26190));
ENDSEC;
END-ISO-10303-21;
